ISO-10303-21;
HEADER;
FILE_DESCRIPTION (('STEP AP214'),
    '1' );
FILE_NAME ('pulley bushing cover.step',
    '2026-10-12T23:53:07',
    ( '' ),
    ( '' ),
    'SwSTEP 2.0',
    'SolidWorks 2024',
    '' );
FILE_SCHEMA (( 'AUTOMOTIVE_DESIGN' ));
ENDSEC;

DATA;
#73=AXIS2_PLACEMENT_3D ( 'NONE', #22419, #1050, #19125 ) ;
#208=ORIENTED_EDGE ( 'NONE', *, *, #30408, .T. ) ;
#252=DIRECTION ( 'NONE',  ( -7.000205099780314469E-17, -1.000000000000000000, 6.590151126658399604E-16 ) ) ;
#279=DIRECTION ( 'NONE',  ( -1.387778780781449620E-15, -6.590151126658398618E-16, -1.000000000000000000 ) ) ;
#414=ORIENTED_EDGE ( 'NONE', *, *, #21024, .T. ) ;
#432=DIRECTION ( 'NONE',  ( -7.000205099780314469E-17, -1.000000000000000000, 6.590151126658399604E-16 ) ) ;
#622=PRODUCT_DEFINITION_SHAPE ( 'NONE', 'NONE',  #17711 ) ;
#895=AXIS2_PLACEMENT_3D ( 'NONE', #6787, #28205, #31908 ) ;
#1014=PRODUCT_DEFINITION_FORMATION_WITH_SPECIFIED_SOURCE ( 'ANY', '', #19635, .NOT_KNOWN. ) ;
#1021=PLANE ( 'NONE',  #32255 ) ;
#1033=EDGE_CURVE ( 'NONE', #31843, #3047, #36000, .T. ) ;
#1050=DIRECTION ( 'NONE',  ( -7.000205099780314469E-17, -1.000000000000000000, 6.590151126658399604E-16 ) ) ;
#1126=( CONVERSION_BASED_UNIT ( 'INCH', #10967 ) LENGTH_UNIT ( ) NAMED_UNIT ( #23398 ) );
#1212=CARTESIAN_POINT ( 'NONE',  ( 0.07499999999999960865, 0.000000000000000000, 0.000000000000000000 ) ) ;
#1234=FACE_OUTER_BOUND ( 'NONE', #16538, .T. ) ;
#1589=DIRECTION ( 'NONE',  ( -1.387778780781449225E-15, 6.590151126658375938E-16, -1.000000000000000000 ) ) ;
#1725=CLOSED_SHELL ( 'NONE', ( #33113, #19688, #19693, #4680, #14913, #20218, #17239, #25799, #22608, #34827, #37384, #3758, #25606 ) ) ;
#1868=DIRECTION ( 'NONE',  ( -7.000205099780314469E-17, -1.000000000000000000, 6.590151126658399604E-16 ) ) ;
#1967=DIRECTION ( 'NONE',  ( -7.000205099780314469E-17, -1.000000000000000000, 6.590151126658399604E-16 ) ) ;
#2139=ORIENTED_EDGE ( 'NONE', *, *, #18885, .F. ) ;
#2222=TOROIDAL_SURFACE ( 'NONE', #33740, 0.1699999999999999845, 0.01499999999999999944 ) ;
#2256=DIRECTION ( 'NONE',  ( 1.387778780781449620E-15, 0.000000000000000000, 1.000000000000000000 ) ) ;
#2815=CIRCLE ( 'NONE', #25823, 0.07499999999999977518 ) ;
#2961=DIRECTION ( 'NONE',  ( 0.000000000000000000, 0.000000000000000000, 1.000000000000000000 ) ) ;
#3047=VERTEX_POINT ( 'NONE', #4799 ) ;
#3051=DIRECTION ( 'NONE',  ( -7.000205099780314469E-17, -1.000000000000000000, 6.590151126658399604E-16 ) ) ;
#3101=DIRECTION ( 'NONE',  ( -1.387778780781449423E-15, 6.590151126658376924E-16, -1.000000000000000000 ) ) ;
#3232=APPLICATION_CONTEXT ( 'configuration controlled 3d designs of mechanical parts and assemblies' ) ;
#3634=AXIS2_PLACEMENT_3D ( 'NONE', #11347, #24519, #8047 ) ;
#3724=FACE_OUTER_BOUND ( 'NONE', #11191, .T. ) ;
#3756=ORIENTED_EDGE ( 'NONE', *, *, #5610, .F. ) ;
#3758=ADVANCED_FACE ( 'NONE', ( #39517 ), #35187, .T. ) ;
#4055=PRODUCT_CONTEXT ( 'NONE', #3232, 'mechanical' ) ;
#4068=DIRECTION ( 'NONE',  ( -7.000205099780314469E-17, -1.000000000000000000, 6.590151126658399604E-16 ) ) ;
#4101=CIRCLE ( 'NONE', #28424, 0.1699999999999995126 ) ;
#4385=VERTEX_POINT ( 'NONE', #31401 ) ;
#4472=FACE_OUTER_BOUND ( 'NONE', #36633, .T. ) ;
#4680=ADVANCED_FACE ( 'NONE', ( #11404 ), #32386, .T. ) ;
#4775=EDGE_LOOP ( 'NONE', ( #22036, #2139, #9198, #29754 ) ) ;
#4799=CARTESIAN_POINT ( 'NONE',  ( -2.359223927328458141E-16, 1.120325691531921079E-16, -0.1699999999999995404 ) ) ;
#4971=AXIS2_PLACEMENT_3D ( 'NONE', #6022, #24573, #8316 ) ;
#5012=DIRECTION ( 'NONE',  ( -1.000000000000000000, 7.000205099780406914E-17, 1.387778780781449620E-15 ) ) ;
#5167=MANIFOLD_SOLID_BREP ( 'Fillet1', #1725 ) ;
#5213=CARTESIAN_POINT ( 'NONE',  ( -2.775557561562891351E-16, -0.05999999999999977573, -0.1999999999999994837 ) ) ;
#5371=ADVANCED_BREP_SHAPE_REPRESENTATION ( '', ( #5167, #27819 ), #11399 ) ;
#5503=CIRCLE ( 'NONE', #17353, 0.1849999999999994982 ) ;
#5574=AXIS2_PLACEMENT_3D ( 'NONE', #9366, #21946, #31400 ) ;
#5610=EDGE_CURVE ( 'NONE', #28969, #22322, #28016, .T. ) ;
#5649=EDGE_LOOP ( 'NONE', ( #13473, #23420, #6721, #11652 ) ) ;
#5793=DIRECTION ( 'NONE',  ( -7.000205099780314469E-17, -1.000000000000000000, 6.590151126658399604E-16 ) ) ;
#5820=CARTESIAN_POINT ( 'NONE',  ( 3.020486921392359971E-16, -1.318030225331671786E-16, 0.1999999999999994837 ) ) ;
#5897=ORIENTED_EDGE ( 'NONE', *, *, #27113, .T. ) ;
#6022=CARTESIAN_POINT ( 'NONE',  ( 0.000000000000000000, 0.000000000000000000, 0.000000000000000000 ) ) ;
#6416=ORIENTED_EDGE ( 'NONE', *, *, #9925, .F. ) ;
#6549=ORIENTED_EDGE ( 'NONE', *, *, #34328, .F. ) ;
#6721=ORIENTED_EDGE ( 'NONE', *, *, #30625, .F. ) ;
#6767=CIRCLE ( 'NONE', #21892, 0.1999999999999994837 ) ;
#6787=CARTESIAN_POINT ( 'NONE',  ( 0.1999999999999989564, -0.05999999999999990757, -5.463695987328526437E-16 ) ) ;
#6947=DIRECTION ( 'NONE',  ( -7.000205099780314469E-17, -1.000000000000000000, 6.590151126658399604E-16 ) ) ;
#7015=EDGE_LOOP ( 'NONE', ( #40483, #19168 ) ) ;
#7207=ORIENTED_EDGE ( 'NONE', *, *, #24228, .F. ) ;
#7296=ORIENTED_EDGE ( 'NONE', *, *, #11295, .F. ) ;
#7332=CIRCLE ( 'NONE', #34313, 0.01500000000000001159 ) ;
#7459=ORIENTED_EDGE ( 'NONE', *, *, #38310, .T. ) ;
#7506=VERTEX_POINT ( 'NONE', #35443 ) ;
#7525=ORIENTED_EDGE ( 'NONE', *, *, #20483, .F. ) ;
#7806=CARTESIAN_POINT ( 'NONE',  ( 0.000000000000000000, -0.01499999999999997689, 0.000000000000000000 ) ) ;
#7962=VERTEX_POINT ( 'NONE', #37626 ) ;
#8047=DIRECTION ( 'NONE',  ( -1.387778780781449423E-15, -6.590151126658397631E-16, -1.000000000000000000 ) ) ;
#8122=AXIS2_PLACEMENT_3D ( 'NONE', #27464, #11626, #8715 ) ;
#8141=DIRECTION ( 'NONE',  ( -1.387778780781449620E-15, 6.590151126658376924E-16, -1.000000000000000000 ) ) ;
#8151=CIRCLE ( 'NONE', #11457, 0.1699999999999995126 ) ;
#8171=CIRCLE ( 'NONE', #31188, 0.1999999999999994837 ) ;
#8235=ORIENTED_EDGE ( 'NONE', *, *, #31080, .F. ) ;
#8315=DIRECTION ( 'NONE',  ( 1.000000000000000000, 0.000000000000000000, 0.000000000000000000 ) ) ;
#8316=DIRECTION ( 'NONE',  ( -1.387778780781449225E-15, 6.590151126658375938E-16, -1.000000000000000000 ) ) ;
#8605=AXIS2_PLACEMENT_3D ( 'NONE', #12911, #22191, #35322 ) ;
#8630=ORIENTED_EDGE ( 'NONE', *, *, #20483, .T. ) ;
#8715=DIRECTION ( 'NONE',  ( -1.387778780781449423E-15, 6.590151126658376924E-16, -1.000000000000000000 ) ) ;
#8920=CARTESIAN_POINT ( 'NONE',  ( 0.000000000000000000, 0.000000000000000000, 0.000000000000000000 ) ) ;
#9108=VERTEX_POINT ( 'NONE', #40209 ) ;
#9198=ORIENTED_EDGE ( 'NONE', *, *, #31080, .T. ) ;
#9270=AXIS2_PLACEMENT_3D ( 'NONE', #24541, #5793, #40357 ) ;
#9366=CARTESIAN_POINT ( 'NONE',  ( 0.07499999999999960865, -0.01500000000000024925, 0.000000000000000000 ) ) ;
#9386=DIRECTION ( 'NONE',  ( -1.387778780781449423E-15, 6.691181741238501047E-16, -1.000000000000000000 ) ) ;
#9406=CARTESIAN_POINT ( 'NONE',  ( -2.775557561562891351E-16, 1.318030225331671786E-16, -0.1999999999999994837 ) ) ;
#9925=EDGE_CURVE ( 'NONE', #17309, #36373, #36902, .T. ) ;
#9983=CIRCLE ( 'NONE', #21801, 0.03000000000000000583 ) ;
#10071=AXIS2_PLACEMENT_3D ( 'NONE', #15579, #28523, #9386 ) ;
#10284=ORIENTED_EDGE ( 'NONE', *, *, #9925, .T. ) ;
#10433=FACE_OUTER_BOUND ( 'NONE', #7015, .T. ) ;
#10596=DIRECTION ( 'NONE',  ( -1.387778780781449423E-15, 6.590151126658376924E-16, -1.000000000000000000 ) ) ;
#10938=VERTEX_POINT ( 'NONE', #11062 ) ;
#10967=LENGTH_MEASURE_WITH_UNIT ( LENGTH_MEASURE( 0.02539999999999999897 ), #38919 );
#11062=CARTESIAN_POINT ( 'NONE',  ( 2.988985998443356465E-16, -0.05999999999999977573, 0.2000000000000000389 ) ) ;
#11065=DIRECTION ( 'NONE',  ( -1.387778780781449423E-15, 6.460451336368206514E-16, -1.000000000000000000 ) ) ;
#11073=ORIENTED_EDGE ( 'NONE', *, *, #34328, .T. ) ;
#11191=EDGE_LOOP ( 'NONE', ( #26132, #11073 ) ) ;
#11208=CARTESIAN_POINT ( 'NONE',  ( 0.000000000000000000, -0.02999999999999995379, 0.000000000000000000 ) ) ;
#11282=ORIENTED_EDGE ( 'NONE', *, *, #23744, .F. ) ;
#11295=EDGE_CURVE ( 'NONE', #35061, #33391, #2815, .T. ) ;
#11299=CARTESIAN_POINT ( 'NONE',  ( 2.988985998443356465E-16, -0.02999999999999982195, 0.2000000000000000389 ) ) ;
#11347=CARTESIAN_POINT ( 'NONE',  ( 0.000000000000000000, -0.02999999999999995379, 0.000000000000000000 ) ) ;
#11399=( GEOMETRIC_REPRESENTATION_CONTEXT ( 3 ) GLOBAL_UNCERTAINTY_ASSIGNED_CONTEXT ( ( #15737 ) ) GLOBAL_UNIT_ASSIGNED_CONTEXT ( ( #1126, #26195, #23112 ) ) REPRESENTATION_CONTEXT ( 'NONE', 'WORKASPACE' ) );
#11404=FACE_OUTER_BOUND ( 'NONE', #5649, .T. ) ;
#11457=AXIS2_PLACEMENT_3D ( 'NONE', #37790, #28322, #34700 ) ;
#11626=DIRECTION ( 'NONE',  ( -7.000205099780314469E-17, -1.000000000000000000, 6.590151126658399604E-16 ) ) ;
#11652=ORIENTED_EDGE ( 'NONE', *, *, #21857, .F. ) ;
#11880=ORIENTED_EDGE ( 'NONE', *, *, #31269, .F. ) ;
#11921=EDGE_LOOP ( 'NONE', ( #11282, #19013, #38537, #36025 ) ) ;
#12401=CARTESIAN_POINT ( 'NONE',  ( -2.567390744445674500E-16, -0.05999999999999978961, -0.1849999999999994982 ) ) ;
#12410=FACE_OUTER_BOUND ( 'NONE', #28802, .T. ) ;
#12422=ORIENTED_EDGE ( 'NONE', *, *, #31269, .T. ) ;
#12458=FACE_BOUND ( 'NONE', #31551, .T. ) ;
#12607=CARTESIAN_POINT ( 'NONE',  ( 0.000000000000000000, 0.000000000000000000, 0.000000000000000000 ) ) ;
#12636=ORIENTED_EDGE ( 'NONE', *, *, #1033, .F. ) ;
#12665=DIRECTION ( 'NONE',  ( 7.000205099780314469E-17, 1.000000000000000000, -6.590151126658399604E-16 ) ) ;
#12751=CARTESIAN_POINT ( 'NONE',  ( 0.000000000000000000, -0.01499999999999997689, 0.000000000000000000 ) ) ;
#12911=CARTESIAN_POINT ( 'NONE',  ( 0.000000000000000000, -0.02999999999999995379, 0.000000000000000000 ) ) ;
#12944=DIRECTION ( 'NONE',  ( -7.000205099780314469E-17, -1.000000000000000000, 6.590151126658399604E-16 ) ) ;
#13112=FACE_BOUND ( 'NONE', #33487, .T. ) ;
#13150=DIRECTION ( 'NONE',  ( -7.000205099780314469E-17, -1.000000000000000000, 6.590151126658399604E-16 ) ) ;
#13473=ORIENTED_EDGE ( 'NONE', *, *, #19055, .T. ) ;
#13530=DIRECTION ( 'NONE',  ( -1.387778780781449423E-15, 6.590151126658375938E-16, -1.000000000000000000 ) ) ;
#13552=DIRECTION ( 'NONE',  ( -7.000205099780314469E-17, -1.000000000000000000, 6.590151126658399604E-16 ) ) ;
#13622=CARTESIAN_POINT ( 'NONE',  ( 2.762449479338929480E-16, -0.05999999999999978961, 0.1849999999999999978 ) ) ;
#13732=DIRECTION ( 'NONE',  ( -1.387778780781449423E-15, 6.590151126658376924E-16, -1.000000000000000000 ) ) ;
#13779=PRODUCT_DEFINITION_CONTEXT ( 'detailed design', #38439, 'design' ) ;
#14114=DIRECTION ( 'NONE',  ( -7.000205099780314469E-17, -1.000000000000000000, 6.590151126658399604E-16 ) ) ;
#14121=DIRECTION ( 'NONE',  ( 7.000205099780314469E-17, 1.000000000000000000, -6.590151126658399604E-16 ) ) ;
#14509=CARTESIAN_POINT ( 'NONE',  ( 2.567413883183506000E-16, -0.03000000000000006481, 0.1699999999999995126 ) ) ;
#14575=VECTOR ( 'NONE', #432, 39.37007874015748143 ) ;
#14728=DIRECTION ( 'NONE',  ( 1.000000000000000000, -7.000205099780415542E-17, -1.510243460696184374E-15 ) ) ;
#14913=ADVANCED_FACE ( 'NONE', ( #24331 ), #21654, .F. ) ;
#15313=ORIENTED_EDGE ( 'NONE', *, *, #24228, .T. ) ;
#15579=CARTESIAN_POINT ( 'NONE',  ( 0.000000000000000000, -0.02999999999999995379, 0.000000000000000000 ) ) ;
#15737=UNCERTAINTY_MEASURE_WITH_UNIT (LENGTH_MEASURE( 1.000000000000000082E-05 ), #1126, 'distance_accuracy_value', 'NONE');
#16096=CIRCLE ( 'NONE', #18047, 0.01500000000000001159 ) ;
#16435=DIRECTION ( 'NONE',  ( -1.387778780781449423E-15, 6.691181741238501047E-16, -1.000000000000000000 ) ) ;
#16438=ORIENTED_EDGE ( 'NONE', *, *, #36308, .F. ) ;
#16449=EDGE_CURVE ( 'NONE', #36513, #7506, #4101, .T. ) ;
#16492=CARTESIAN_POINT ( 'NONE',  ( 0.000000000000000000, -0.05999999999999990757, 0.000000000000000000 ) ) ;
#16538=EDGE_LOOP ( 'NONE', ( #6416, #5897, #38046, #8235 ) ) ;
#16704=DIRECTION ( 'NONE',  ( -7.000205099780314469E-17, -1.000000000000000000, 6.590151126658399604E-16 ) ) ;
#16767=EDGE_LOOP ( 'NONE', ( #11880, #19144, #21586, #7525 ) ) ;
#17239=ADVANCED_FACE ( 'NONE', ( #30484, #3724 ), #21642, .F. ) ;
#17289=AXIS2_PLACEMENT_3D ( 'NONE', #23228, #4068, #19714 ) ;
#17309=VERTEX_POINT ( 'NONE', #28621 ) ;
#17353=AXIS2_PLACEMENT_3D ( 'NONE', #38041, #22232, #16435 ) ;
#17616=CARTESIAN_POINT ( 'NONE',  ( 0.000000000000000000, 0.000000000000000000, 0.000000000000000000 ) ) ;
#17692=ORIENTED_EDGE ( 'NONE', *, *, #19987, .T. ) ;
#17701=ORIENTED_EDGE ( 'NONE', *, *, #18023, .F. ) ;
#17711=PRODUCT_DEFINITION ( 'UNKNOWN', '', #1014, #13779 ) ;
#17750=ORIENTED_EDGE ( 'NONE', *, *, #16449, .F. ) ;
#17849=LINE ( 'NONE', #24863, #39476 ) ;
#17966=CARTESIAN_POINT ( 'NONE',  ( -2.359223927328458141E-16, -0.02999999999999984276, -0.1699999999999995404 ) ) ;
#18023=EDGE_CURVE ( 'NONE', #28184, #10938, #27859, .T. ) ;
#18047=AXIS2_PLACEMENT_3D ( 'NONE', #14509, #14728, #20714 ) ;
#18380=DIRECTION ( 'NONE',  ( -7.000205099780314469E-17, -1.000000000000000000, 6.590151126658399604E-16 ) ) ;
#18432=VECTOR ( 'NONE', #21983, 39.37007874015748143 ) ;
#18596=SHAPE_DEFINITION_REPRESENTATION ( #622, #24383 ) ;
#18810=EDGE_CURVE ( 'NONE', #3047, #31843, #31068, .T. ) ;
#18825=AXIS2_PLACEMENT_3D ( 'NONE', #26713, #23012, #11065 ) ;
#18885=EDGE_CURVE ( 'NONE', #36373, #17309, #38275, .T. ) ;
#19013=ORIENTED_EDGE ( 'NONE', *, *, #18810, .F. ) ;
#19055=EDGE_CURVE ( 'NONE', #9108, #28184, #6767, .T. ) ;
#19125=DIRECTION ( 'NONE',  ( -1.387778780781449423E-15, 6.460451336368206514E-16, -1.000000000000000000 ) ) ;
#19144=ORIENTED_EDGE ( 'NONE', *, *, #21024, .F. ) ;
#19168=ORIENTED_EDGE ( 'NONE', *, *, #1033, .T. ) ;
#19180=AXIS2_PLACEMENT_3D ( 'NONE', #34758, #37646, #3101 ) ;
#19270=AXIS2_PLACEMENT_3D ( 'NONE', #28307, #12665, #28120 ) ;
#19276=AXIS2_PLACEMENT_3D ( 'NONE', #19523, #12944, #32057 ) ;
#19306=CARTESIAN_POINT ( 'NONE',  ( 1.132682595522134681E-16, -4.942613344993767655E-17, 0.07499999999999977518 ) ) ;
#19523=CARTESIAN_POINT ( 'NONE',  ( 0.000000000000000000, -0.05999999999999990757, 0.000000000000000000 ) ) ;
#19635=PRODUCT ( 'pulley bushing cover', 'pulley bushing cover', '', ( #4055 ) ) ;
#19688=ADVANCED_FACE ( 'NONE', ( #4472 ), #39630, .T. ) ;
#19693=ADVANCED_FACE ( 'NONE', ( #1234 ), #36149, .F. ) ;
#19714=DIRECTION ( 'NONE',  ( -1.387778780781449423E-15, -6.590151126658397631E-16, -1.000000000000000000 ) ) ;
#19886=FACE_OUTER_BOUND ( 'NONE', #33380, .T. ) ;
#19987=EDGE_CURVE ( 'NONE', #7962, #4385, #28473, .T. ) ;
#20043=VERTEX_POINT ( 'NONE', #5213 ) ;
#20218=ADVANCED_FACE ( 'NONE', ( #12410 ), #34208, .F. ) ;
#20245=AXIS2_PLACEMENT_3D ( 'NONE', #17616, #14121, #8141 ) ;
#20376=DIRECTION ( 'NONE',  ( -1.387778780781449423E-15, 6.545052484820649979E-16, -1.000000000000000000 ) ) ;
#20471=CYLINDRICAL_SURFACE ( 'NONE', #8122, 0.07499999999999977518 ) ;
#20483=EDGE_CURVE ( 'NONE', #4385, #7962, #5503, .T. ) ;
#20597=EDGE_LOOP ( 'NONE', ( #17692, #7459, #21156, #39049 ) ) ;
#20694=ORIENTED_EDGE ( 'NONE', *, *, #26761, .F. ) ;
#20704=VECTOR ( 'NONE', #13150, 39.37007874015748143 ) ;
#20714=DIRECTION ( 'NONE',  ( -1.510243460696182204E-15, 0.000000000000000000, -1.000000000000000000 ) ) ;
#21024=EDGE_CURVE ( 'NONE', #7506, #36513, #8151, .T. ) ;
#21126=FACE_OUTER_BOUND ( 'NONE', #36114, .T. ) ;
#21156=ORIENTED_EDGE ( 'NONE', *, *, #5610, .T. ) ;
#21586=ORIENTED_EDGE ( 'NONE', *, *, #26761, .T. ) ;
#21642=PLANE ( 'NONE',  #895 ) ;
#21654=CYLINDRICAL_SURFACE ( 'NONE', #9270, 0.1849999999999994982 ) ;
#21693=CIRCLE ( 'NONE', #73, 0.1849999999999994982 ) ;
#21801=AXIS2_PLACEMENT_3D ( 'NONE', #24935, #21861, #34388 ) ;
#21817=ORIENTED_EDGE ( 'NONE', *, *, #19987, .F. ) ;
#21857=EDGE_CURVE ( 'NONE', #9108, #20043, #37584, .T. ) ;
#21861=DIRECTION ( 'NONE',  ( 1.000000000000000000, -7.000205099780415542E-17, -1.510243460696184374E-15 ) ) ;
#21892=AXIS2_PLACEMENT_3D ( 'NONE', #11208, #1967, #36709 ) ;
#21946=DIRECTION ( 'NONE',  ( -7.000205099780496893E-17, -1.000000000000000000, -6.590151126658374952E-16 ) ) ;
#21983=DIRECTION ( 'NONE',  ( -7.000205099780314469E-17, -1.000000000000000000, 6.590151126658399604E-16 ) ) ;
#22036=ORIENTED_EDGE ( 'NONE', *, *, #27113, .F. ) ;
#22191=DIRECTION ( 'NONE',  ( -7.000205099780314469E-17, -1.000000000000000000, 6.590151126658399604E-16 ) ) ;
#22232=DIRECTION ( 'NONE',  ( 7.000205099780314469E-17, 1.000000000000000000, -6.590151126658399604E-16 ) ) ;
#22322=VERTEX_POINT ( 'NONE', #12401 ) ;
#22419=CARTESIAN_POINT ( 'NONE',  ( 0.000000000000000000, -0.05999999999999990757, 0.000000000000000000 ) ) ;
#22608=ADVANCED_FACE ( 'NONE', ( #10433, #13112 ), #1021, .F. ) ;
#23012=DIRECTION ( 'NONE',  ( -7.000205099780314469E-17, -1.000000000000000000, 6.590151126658399604E-16 ) ) ;
#23112=( NAMED_UNIT ( * ) SI_UNIT ( $, .STERADIAN. ) SOLID_ANGLE_UNIT ( ) );
#23228=CARTESIAN_POINT ( 'NONE',  ( 0.000000000000000000, -0.02999999999999995379, 0.000000000000000000 ) ) ;
#23318=CIRCLE ( 'NONE', #36412, 0.03000000000000000583 ) ;
#23398=DIMENSIONAL_EXPONENTS ( 1.000000000000000000, 0.000000000000000000, 0.000000000000000000, 0.000000000000000000, 0.000000000000000000, 0.000000000000000000, 0.000000000000000000 ) ;
#23420=ORIENTED_EDGE ( 'NONE', *, *, #18023, .T. ) ;
#23433=CARTESIAN_POINT ( 'NONE',  ( 0.000000000000000000, -0.01499999999999997689, 0.000000000000000000 ) ) ;
#23620=DIRECTION ( 'NONE',  ( -1.387778780781449423E-15, 6.545052484820649979E-16, -1.000000000000000000 ) ) ;
#23744=EDGE_CURVE ( 'NONE', #31843, #28184, #9983, .T. ) ;
#24228=EDGE_CURVE ( 'NONE', #22322, #28969, #21693, .T. ) ;
#24331=FACE_OUTER_BOUND ( 'NONE', #20597, .T. ) ;
#24383=SHAPE_REPRESENTATION ( 'pulley bushing cover', ( #27819 ), #11399 ) ;
#24519=DIRECTION ( 'NONE',  ( -7.000205099780314469E-17, -1.000000000000000000, 6.590151126658399604E-16 ) ) ;
#24541=CARTESIAN_POINT ( 'NONE',  ( 0.000000000000000000, 0.000000000000000000, 0.000000000000000000 ) ) ;
#24573=DIRECTION ( 'NONE',  ( -7.000205099780314469E-17, -1.000000000000000000, 6.590151126658399604E-16 ) ) ;
#24585=AXIS2_PLACEMENT_3D ( 'NONE', #12607, #28064, #34628 ) ;
#24863=CARTESIAN_POINT ( 'NONE',  ( -2.567390744445674500E-16, 1.219177958431796432E-16, -0.1849999999999994982 ) ) ;
#24935=CARTESIAN_POINT ( 'NONE',  ( 2.567413883183506493E-16, -0.03000000000000006481, 0.1699999999999995404 ) ) ;
#24948=DIRECTION ( 'NONE',  ( -7.000205099780314469E-17, -1.000000000000000000, 6.590151126658399604E-16 ) ) ;
#25012=PLANE ( 'NONE',  #5574 ) ;
#25029=ORIENTED_EDGE ( 'NONE', *, *, #19055, .F. ) ;
#25136=VECTOR ( 'NONE', #18380, 39.37007874015748143 ) ;
#25167=AXIS2_PLACEMENT_3D ( 'NONE', #25852, #38170, #10596 ) ;
#25273=CIRCLE ( 'NONE', #19276, 0.1999999999999994837 ) ;
#25313=DIRECTION ( 'NONE',  ( -1.387778780781449620E-15, 6.528313220153589231E-16, -1.000000000000000000 ) ) ;
#25513=EDGE_CURVE ( 'NONE', #7962, #22322, #17849, .T. ) ;
#25606=ADVANCED_FACE ( 'NONE', ( #26081 ), #26369, .F. ) ;
#25799=ADVANCED_FACE ( 'NONE', ( #19886 ), #27072, .T. ) ;
#25823=AXIS2_PLACEMENT_3D ( 'NONE', #7806, #1868, #20376 ) ;
#25852=CARTESIAN_POINT ( 'NONE',  ( 0.000000000000000000, 0.000000000000000000, 0.000000000000000000 ) ) ;
#25922=ORIENTED_EDGE ( 'NONE', *, *, #16449, .T. ) ;
#26081=FACE_OUTER_BOUND ( 'NONE', #16767, .T. ) ;
#26132=ORIENTED_EDGE ( 'NONE', *, *, #30625, .T. ) ;
#26195=( NAMED_UNIT ( * ) PLANE_ANGLE_UNIT ( ) SI_UNIT ( $, .RADIAN. ) );
#26369=TOROIDAL_SURFACE ( 'NONE', #8605, 0.1699999999999999845, 0.01499999999999999944 ) ;
#26596=CARTESIAN_POINT ( 'NONE',  ( 2.685932296560563025E-16, -0.01499999999999986587, 0.1699999999999999845 ) ) ;
#26713=CARTESIAN_POINT ( 'NONE',  ( 0.000000000000000000, -0.05999999999999990757, 0.000000000000000000 ) ) ;
#26761=EDGE_CURVE ( 'NONE', #7506, #7962, #7332, .T. ) ;
#27072=CYLINDRICAL_SURFACE ( 'NONE', #32957, 0.1999999999999994837 ) ;
#27113=EDGE_CURVE ( 'NONE', #17309, #35061, #31639, .T. ) ;
#27256=CIRCLE ( 'NONE', #32487, 0.1999999999999994837 ) ;
#27328=VECTOR ( 'NONE', #6947, 39.37007874015748143 ) ;
#27464=CARTESIAN_POINT ( 'NONE',  ( 0.000000000000000000, 0.000000000000000000, 0.000000000000000000 ) ) ;
#27819=AXIS2_PLACEMENT_3D ( 'NONE', #8920, #2961, #8315 ) ;
#27859=LINE ( 'NONE', #5820, #25136 ) ;
#28016=CIRCLE ( 'NONE', #18825, 0.1849999999999994982 ) ;
#28064=DIRECTION ( 'NONE',  ( -7.000205099780314469E-17, -1.000000000000000000, 6.590151126658399604E-16 ) ) ;
#28120=DIRECTION ( 'NONE',  ( -1.387778780781449620E-15, 6.590151126658376924E-16, -1.000000000000000000 ) ) ;
#28178=ORIENTED_EDGE ( 'NONE', *, *, #23744, .T. ) ;
#28184=VERTEX_POINT ( 'NONE', #11299 ) ;
#28190=CARTESIAN_POINT ( 'NONE',  ( -1.040834085586084010E-16, 4.942613344993767655E-17, -0.07499999999999977518 ) ) ;
#28205=DIRECTION ( 'NONE',  ( 7.000205099780496893E-17, 1.000000000000000000, 6.590151126658374952E-16 ) ) ;
#28307=CARTESIAN_POINT ( 'NONE',  ( 0.000000000000000000, 0.000000000000000000, 0.000000000000000000 ) ) ;
#28322=DIRECTION ( 'NONE',  ( -7.000205099780314469E-17, -1.000000000000000000, 6.590151126658399604E-16 ) ) ;
#28424=AXIS2_PLACEMENT_3D ( 'NONE', #12751, #252, #25313 ) ;
#28473=CIRCLE ( 'NONE', #10071, 0.1849999999999994982 ) ;
#28523=DIRECTION ( 'NONE',  ( 7.000205099780314469E-17, 1.000000000000000000, -6.590151126658399604E-16 ) ) ;
#28621=CARTESIAN_POINT ( 'NONE',  ( 1.127432441697302489E-16, 4.942613344993744236E-17, 0.07499999999999998335 ) ) ;
#28802=EDGE_LOOP ( 'NONE', ( #33747, #8630, #29300, #15313 ) ) ;
#28816=FACE_OUTER_BOUND ( 'NONE', #38734, .T. ) ;
#28843=DIRECTION ( 'NONE',  ( -1.387778780781449225E-15, 6.402768735150633127E-16, -1.000000000000000000 ) ) ;
#28969=VERTEX_POINT ( 'NONE', #13622 ) ;
#29300=ORIENTED_EDGE ( 'NONE', *, *, #25513, .T. ) ;
#29754=ORIENTED_EDGE ( 'NONE', *, *, #38600, .T. ) ;
#30027=CARTESIAN_POINT ( 'NONE',  ( 2.804450709937611668E-16, 1.120325691531909986E-16, 0.1700000000000000400 ) ) ;
#30408=EDGE_CURVE ( 'NONE', #28184, #9108, #27256, .T. ) ;
#30484=FACE_BOUND ( 'NONE', #34547, .T. ) ;
#30527=DIRECTION ( 'NONE',  ( 1.387778780781449225E-15, 0.000000000000000000, 1.000000000000000000 ) ) ;
#30625=EDGE_CURVE ( 'NONE', #20043, #10938, #8171, .T. ) ;
#31068=CIRCLE ( 'NONE', #19270, 0.1699999999999995404 ) ;
#31080=EDGE_CURVE ( 'NONE', #36373, #33391, #34757, .T. ) ;
#31188=AXIS2_PLACEMENT_3D ( 'NONE', #16492, #16704, #28843 ) ;
#31269=EDGE_CURVE ( 'NONE', #36513, #4385, #16096, .T. ) ;
#31350=CARTESIAN_POINT ( 'NONE',  ( -1.040834085586084010E-16, 4.942613344993767655E-17, -0.07499999999999977518 ) ) ;
#31400=DIRECTION ( 'NONE',  ( -1.387778780781449423E-15, 6.590151126658375938E-16, -1.000000000000000000 ) ) ;
#31401=CARTESIAN_POINT ( 'NONE',  ( 2.762449479338929480E-16, -0.02999999999999982889, 0.1849999999999999978 ) ) ;
#31551=EDGE_LOOP ( 'NONE', ( #32869, #7296 ) ) ;
#31639=LINE ( 'NONE', #19306, #14575 ) ;
#31843=VERTEX_POINT ( 'NONE', #30027 ) ;
#31908=DIRECTION ( 'NONE',  ( 1.387778780781449423E-15, -6.590151126658375938E-16, 1.000000000000000000 ) ) ;
#32052=CARTESIAN_POINT ( 'NONE',  ( 2.793950402287933479E-16, -1.219177958431796432E-16, 0.1849999999999994982 ) ) ;
#32057=DIRECTION ( 'NONE',  ( -1.387778780781449225E-15, 6.402768735150633127E-16, -1.000000000000000000 ) ) ;
#32099=CARTESIAN_POINT ( 'NONE',  ( 0.000000000000000000, -0.02999999999999995379, 0.000000000000000000 ) ) ;
#32234=LINE ( 'NONE', #32052, #27328 ) ;
#32255=AXIS2_PLACEMENT_3D ( 'NONE', #1212, #38799, #13530 ) ;
#32386=CYLINDRICAL_SURFACE ( 'NONE', #4971, 0.1999999999999994837 ) ;
#32409=ORIENTED_EDGE ( 'NONE', *, *, #18885, .T. ) ;
#32422=CARTESIAN_POINT ( 'NONE',  ( 0.000000000000000000, 0.000000000000000000, 0.000000000000000000 ) ) ;
#32487=AXIS2_PLACEMENT_3D ( 'NONE', #39964, #24948, #33999 ) ;
#32869=ORIENTED_EDGE ( 'NONE', *, *, #38600, .F. ) ;
#32957=AXIS2_PLACEMENT_3D ( 'NONE', #32422, #14114, #1589 ) ;
#33113=ADVANCED_FACE ( 'NONE', ( #28816 ), #2222, .F. ) ;
#33380=EDGE_LOOP ( 'NONE', ( #17701, #208, #36366, #6549 ) ) ;
#33391=VERTEX_POINT ( 'NONE', #39678 ) ;
#33487=EDGE_LOOP ( 'NONE', ( #32409, #10284 ) ) ;
#33740=AXIS2_PLACEMENT_3D ( 'NONE', #32099, #37661, #279 ) ;
#33747=ORIENTED_EDGE ( 'NONE', *, *, #38310, .F. ) ;
#33999=DIRECTION ( 'NONE',  ( -1.387778780781449225E-15, 6.616194359655655447E-16, -1.000000000000000000 ) ) ;
#34208=CYLINDRICAL_SURFACE ( 'NONE', #24585, 0.1849999999999994982 ) ;
#34313=AXIS2_PLACEMENT_3D ( 'NONE', #36388, #39674, #2256 ) ;
#34328=EDGE_CURVE ( 'NONE', #10938, #20043, #25273, .T. ) ;
#34388=DIRECTION ( 'NONE',  ( -1.510243460696184176E-15, 0.000000000000000000, -1.000000000000000000 ) ) ;
#34547=EDGE_LOOP ( 'NONE', ( #7207, #3756 ) ) ;
#34576=CIRCLE ( 'NONE', #38502, 0.07499999999999977518 ) ;
#34628=DIRECTION ( 'NONE',  ( -1.387778780781449423E-15, 6.590151126658376924E-16, -1.000000000000000000 ) ) ;
#34700=DIRECTION ( 'NONE',  ( -1.387778780781449620E-15, 6.528313220153589231E-16, -1.000000000000000000 ) ) ;
#34757=LINE ( 'NONE', #28190, #20704 ) ;
#34758=CARTESIAN_POINT ( 'NONE',  ( 0.000000000000000000, 0.000000000000000000, 0.000000000000000000 ) ) ;
#34827=ADVANCED_FACE ( 'NONE', ( #35696 ), #20471, .F. ) ;
#35061=VERTEX_POINT ( 'NONE', #35802 ) ;
#35187=TOROIDAL_SURFACE ( 'NONE', #3634, 0.1700000000000000400, 0.02999999999999999889 ) ;
#35322=DIRECTION ( 'NONE',  ( -1.387778780781449620E-15, -6.590151126658398618E-16, -1.000000000000000000 ) ) ;
#35443=CARTESIAN_POINT ( 'NONE',  ( -2.359223927328457648E-16, -0.01499999999999986587, -0.1699999999999995126 ) ) ;
#35696=FACE_OUTER_BOUND ( 'NONE', #4775, .T. ) ;
#35802=CARTESIAN_POINT ( 'NONE',  ( 1.127432441697302489E-16, -0.01499999999999992832, 0.07499999999999998335 ) ) ;
#36000=CIRCLE ( 'NONE', #20245, 0.1699999999999995404 ) ;
#36025=ORIENTED_EDGE ( 'NONE', *, *, #30408, .F. ) ;
#36043=SHAPE_REPRESENTATION_RELATIONSHIP ( 'NONE' , 'NONE' ,  #24383, #5371 ) ;
#36114=EDGE_LOOP ( 'NONE', ( #414, #25922 ) ) ;
#36149=CYLINDRICAL_SURFACE ( 'NONE', #36343, 0.07499999999999977518 ) ;
#36308=EDGE_CURVE ( 'NONE', #3047, #9108, #23318, .T. ) ;
#36343=AXIS2_PLACEMENT_3D ( 'NONE', #38434, #13552, #13732 ) ;
#36366=ORIENTED_EDGE ( 'NONE', *, *, #21857, .T. ) ;
#36373=VERTEX_POINT ( 'NONE', #31350 ) ;
#36388=CARTESIAN_POINT ( 'NONE',  ( -2.359223927328457648E-16, -0.02999999999999984276, -0.1699999999999995126 ) ) ;
#36412=AXIS2_PLACEMENT_3D ( 'NONE', #17966, #5012, #30527 ) ;
#36513=VERTEX_POINT ( 'NONE', #26596 ) ;
#36633=EDGE_LOOP ( 'NONE', ( #12636, #28178, #25029, #16438 ) ) ;
#36709=DIRECTION ( 'NONE',  ( -1.387778780781449225E-15, 6.616194359655655447E-16, -1.000000000000000000 ) ) ;
#36902=CIRCLE ( 'NONE', #19180, 0.07499999999999977518 ) ;
#37384=ADVANCED_FACE ( 'NONE', ( #21126, #12458 ), #25012, .T. ) ;
#37584=LINE ( 'NONE', #9406, #18432 ) ;
#37626=CARTESIAN_POINT ( 'NONE',  ( -2.567390744445674500E-16, -0.02999999999999982889, -0.1849999999999994982 ) ) ;
#37646=DIRECTION ( 'NONE',  ( -7.000205099780314469E-17, -1.000000000000000000, 6.590151126658399604E-16 ) ) ;
#37661=DIRECTION ( 'NONE',  ( -7.000205099780314469E-17, -1.000000000000000000, 6.590151126658399604E-16 ) ) ;
#37790=CARTESIAN_POINT ( 'NONE',  ( 0.000000000000000000, -0.01499999999999997689, 0.000000000000000000 ) ) ;
#38041=CARTESIAN_POINT ( 'NONE',  ( 0.000000000000000000, -0.02999999999999995379, 0.000000000000000000 ) ) ;
#38046=ORIENTED_EDGE ( 'NONE', *, *, #11295, .T. ) ;
#38170=DIRECTION ( 'NONE',  ( -7.000205099780314469E-17, -1.000000000000000000, 6.590151126658399604E-16 ) ) ;
#38275=CIRCLE ( 'NONE', #25167, 0.07499999999999977518 ) ;
#38310=EDGE_CURVE ( 'NONE', #4385, #28969, #32234, .T. ) ;
#38434=CARTESIAN_POINT ( 'NONE',  ( 0.000000000000000000, 0.000000000000000000, 0.000000000000000000 ) ) ;
#38439=APPLICATION_CONTEXT ( 'configuration controlled 3d designs of mechanical parts and assemblies' ) ;
#38502=AXIS2_PLACEMENT_3D ( 'NONE', #23433, #39631, #23620 ) ;
#38537=ORIENTED_EDGE ( 'NONE', *, *, #36308, .T. ) ;
#38600=EDGE_CURVE ( 'NONE', #33391, #35061, #34576, .T. ) ;
#38734=EDGE_LOOP ( 'NONE', ( #17750, #12422, #21817, #20694 ) ) ;
#38799=DIRECTION ( 'NONE',  ( -7.000205099780496893E-17, -1.000000000000000000, -6.590151126658374952E-16 ) ) ;
#38919=( LENGTH_UNIT ( ) NAMED_UNIT ( * ) SI_UNIT ( $, .METRE. ) );
#39049=ORIENTED_EDGE ( 'NONE', *, *, #25513, .F. ) ;
#39476=VECTOR ( 'NONE', #3051, 39.37007874015748143 ) ;
#39517=FACE_OUTER_BOUND ( 'NONE', #11921, .T. ) ;
#39630=TOROIDAL_SURFACE ( 'NONE', #17289, 0.1700000000000000400, 0.02999999999999999889 ) ;
#39631=DIRECTION ( 'NONE',  ( -7.000205099780314469E-17, -1.000000000000000000, 6.590151126658399604E-16 ) ) ;
#39674=DIRECTION ( 'NONE',  ( -1.000000000000000000, 7.000205099780406914E-17, 1.387778780781449620E-15 ) ) ;
#39678=CARTESIAN_POINT ( 'NONE',  ( -1.040834085586084010E-16, -0.01499999999999992832, -0.07499999999999977518 ) ) ;
#39964=CARTESIAN_POINT ( 'NONE',  ( 0.000000000000000000, -0.02999999999999995379, 0.000000000000000000 ) ) ;
#40209=CARTESIAN_POINT ( 'NONE',  ( -2.775557561562891351E-16, -0.02999999999999982195, -0.1999999999999994837 ) ) ;
#40357=DIRECTION ( 'NONE',  ( -1.387778780781449423E-15, 6.590151126658376924E-16, -1.000000000000000000 ) ) ;
#40483=ORIENTED_EDGE ( 'NONE', *, *, #18810, .T. ) ;
#40674=COLOUR_RGB('Light Blue',0.38,0.62,0.78);
#40675=FILL_AREA_STYLE_COLOUR('',#40674);
#40676=FILL_AREA_STYLE('',(#40675));
#40677=SURFACE_STYLE_FILL_AREA(#40676);
#40678=SURFACE_SIDE_STYLE('',(#40677));
#40679=SURFACE_STYLE_USAGE(.BOTH.,#40678);
#40680=PRESENTATION_STYLE_ASSIGNMENT((#40679));
#40720=STYLED_ITEM('',(#40680),#5167);
#40721=MECHANICAL_DESIGN_GEOMETRIC_PRESENTATION_REPRESENTATION('',(#40720),#11399);
ENDSEC;
END-ISO-10303-21;
